ISO-10303-21;
HEADER;
/* Generated by software containing ST-Developer
 * from STEP Tools, Inc. (www.steptools.com) 
 */

FILE_DESCRIPTION(
/* description */ ('Bin tilter linkage'),
/* implementation_level */ '2;1');

FILE_NAME(
/* name */ 'M4 short cap screw (14).step',
/* time_stamp */ '2026-10-28T03:26:24-07:00',
/* author */ (''),
/* organization */ (''),
/* preprocessor_version */ 'ST-DEVELOPER v20.2',
/* originating_system */ 'Autodesk Translation Framework v15.17.0.0',
/* authorisation */ '');

FILE_SCHEMA (('AUTOMOTIVE_DESIGN { 1 0 10303 214 3 1 1 }'));
ENDSEC;

DATA;
#10=MECHANICAL_DESIGN_GEOMETRIC_PRESENTATION_REPRESENTATION('',(#911),#23728);
#699=SHAPE_REPRESENTATION_RELATIONSHIP('SRR','None',#24164,#805);
#805=ADVANCED_BREP_SHAPE_REPRESENTATION('',(#1024),#23664);
#911=STYLED_ITEM('',(#24772),#1024);
#1024=MANIFOLD_SOLID_BREP('Body1',#12442);
#1308=FACE_BOUND('',#3256,.T.);
#1671=PLANE('',#14468);
#1672=PLANE('',#14473);
#1673=PLANE('',#14476);
#2257=FACE_OUTER_BOUND('',#3255,.T.);
#2258=FACE_OUTER_BOUND('',#3257,.T.);
#2259=FACE_OUTER_BOUND('',#3258,.T.);
#2260=FACE_OUTER_BOUND('',#3259,.T.);
#2261=FACE_OUTER_BOUND('',#3260,.T.);
#3255=EDGE_LOOP('',(#9769));
#3256=EDGE_LOOP('',(#9770));
#3257=EDGE_LOOP('',(#9771,#9772,#9773,#9774));
#3258=EDGE_LOOP('',(#9775));
#3259=EDGE_LOOP('',(#9776,#9777,#9778,#9779));
#3260=EDGE_LOOP('',(#9780));
#4175=LINE('',#21335,#4850);
#4176=LINE('',#21339,#4851);
#4850=VECTOR('',#17394,0.35);
#4851=VECTOR('',#17399,0.199999999999999);
#5571=CIRCLE('',#14469,0.35);
#5572=CIRCLE('',#14470,0.199999999999999);
#5573=CIRCLE('',#14472,0.35);
#5574=CIRCLE('',#14475,0.199999999999999);
#6421=VERTEX_POINT('',#21328);
#6422=VERTEX_POINT('',#21330);
#6423=VERTEX_POINT('',#21333);
#6424=VERTEX_POINT('',#21338);
#7624=EDGE_CURVE('',#6421,#6421,#5571,.T.);
#7625=EDGE_CURVE('',#6422,#6422,#5572,.T.);
#7626=EDGE_CURVE('',#6423,#6423,#5573,.T.);
#7627=EDGE_CURVE('',#6423,#6421,#4175,.T.);
#7628=EDGE_CURVE('',#6422,#6424,#4176,.T.);
#7629=EDGE_CURVE('',#6424,#6424,#5574,.T.);
#9769=ORIENTED_EDGE('',*,*,#7624,.F.);
#9770=ORIENTED_EDGE('',*,*,#7625,.T.);
#9771=ORIENTED_EDGE('',*,*,#7626,.F.);
#9772=ORIENTED_EDGE('',*,*,#7627,.T.);
#9773=ORIENTED_EDGE('',*,*,#7624,.T.);
#9774=ORIENTED_EDGE('',*,*,#7627,.F.);
#9775=ORIENTED_EDGE('',*,*,#7626,.T.);
#9776=ORIENTED_EDGE('',*,*,#7625,.F.);
#9777=ORIENTED_EDGE('',*,*,#7628,.T.);
#9778=ORIENTED_EDGE('',*,*,#7629,.T.);
#9779=ORIENTED_EDGE('',*,*,#7628,.F.);
#9780=ORIENTED_EDGE('',*,*,#7629,.F.);
#11451=CYLINDRICAL_SURFACE('',#14471,0.35);
#11452=CYLINDRICAL_SURFACE('',#14474,0.199999999999999);
#11982=ADVANCED_FACE('',(#2257,#1308),#1671,.F.);
#11983=ADVANCED_FACE('',(#2258),#11451,.T.);
#11984=ADVANCED_FACE('',(#2259),#1672,.T.);
#11985=ADVANCED_FACE('',(#2260),#11452,.T.);
#11986=ADVANCED_FACE('',(#2261),#1673,.F.);
#12442=CLOSED_SHELL('',(#11982,#11983,#11984,#11985,#11986));
#14467=AXIS2_PLACEMENT_3D('',#21326,#17382,#17383);
#14468=AXIS2_PLACEMENT_3D('',#21327,#17384,#17385);
#14469=AXIS2_PLACEMENT_3D('',#21329,#17386,#17387);
#14470=AXIS2_PLACEMENT_3D('',#21331,#17388,#17389);
#14471=AXIS2_PLACEMENT_3D('',#21332,#17390,#17391);
#14472=AXIS2_PLACEMENT_3D('',#21334,#17392,#17393);
#14473=AXIS2_PLACEMENT_3D('',#21336,#17395,#17396);
#14474=AXIS2_PLACEMENT_3D('',#21337,#17397,#17398);
#14475=AXIS2_PLACEMENT_3D('',#21340,#17400,#17401);
#14476=AXIS2_PLACEMENT_3D('',#21341,#17402,#17403);
#17382=DIRECTION('axis',(0.,0.,1.));
#17383=DIRECTION('refdir',(1.,0.,0.));
#17384=DIRECTION('center_axis',(0.,1.,0.));
#17385=DIRECTION('ref_axis',(1.,0.,0.));
#17386=DIRECTION('center_axis',(0.,1.,0.));
#17387=DIRECTION('ref_axis',(1.,0.,0.));
#17388=DIRECTION('center_axis',(0.,1.,0.));
#17389=DIRECTION('ref_axis',(1.,0.,0.));
#17390=DIRECTION('center_axis',(0.,1.,0.));
#17391=DIRECTION('ref_axis',(1.,0.,0.));
#17392=DIRECTION('center_axis',(0.,1.,0.));
#17393=DIRECTION('ref_axis',(1.,0.,0.));
#17394=DIRECTION('',(0.,-1.,0.));
#17395=DIRECTION('center_axis',(0.,1.,0.));
#17396=DIRECTION('ref_axis',(1.,0.,0.));
#17397=DIRECTION('center_axis',(0.,1.,0.));
#17398=DIRECTION('ref_axis',(1.,0.,0.));
#17399=DIRECTION('',(0.,-1.,0.));
#17400=DIRECTION('center_axis',(0.,1.,0.));
#17401=DIRECTION('ref_axis',(1.,0.,0.));
#17402=DIRECTION('center_axis',(0.,1.,0.));
#17403=DIRECTION('ref_axis',(1.,0.,0.));
#21326=CARTESIAN_POINT('',(0.,0.,0.));
#21327=CARTESIAN_POINT('Origin',(8.08877866266397,0.8,17.1120538880616));
#21328=CARTESIAN_POINT('',(7.73877866266397,0.8,17.1120538880616));
#21329=CARTESIAN_POINT('Origin',(8.08877866266397,0.8,17.1120538880616));
#21330=CARTESIAN_POINT('',(7.88877866266397,0.8,17.1120538880616));
#21331=CARTESIAN_POINT('Origin',(8.08877866266397,0.8,17.1120538880616));
#21332=CARTESIAN_POINT('Origin',(8.08877866266397,0.8,17.1120538880616));
#21333=CARTESIAN_POINT('',(7.73877866266397,1.2,17.1120538880616));
#21334=CARTESIAN_POINT('Origin',(8.08877866266397,1.2,17.1120538880616));
#21335=CARTESIAN_POINT('',(7.73877866266397,0.8,17.1120538880616));
#21336=CARTESIAN_POINT('Origin',(8.08877866266397,1.2,17.1120538880616));
#21337=CARTESIAN_POINT('Origin',(8.08877866266397,0.1,17.1120538880616));
#21338=CARTESIAN_POINT('',(7.88877866266397,0.1,17.1120538880616));
#21339=CARTESIAN_POINT('',(7.88877866266397,0.1,17.1120538880616));
#21340=CARTESIAN_POINT('Origin',(8.08877866266397,0.1,17.1120538880616));
#21341=CARTESIAN_POINT('Origin',(8.08877866266397,0.1,17.1120538880616));
#23547=UNCERTAINTY_MEASURE_WITH_UNIT(LENGTH_MEASURE(0.001),#23729,
'DISTANCE_ACCURACY_VALUE',
'Maximum model space distance between geometric entities at asserted c
onnectivities');
#23611=UNCERTAINTY_MEASURE_WITH_UNIT(LENGTH_MEASURE(0.001),#23729,
'DISTANCE_ACCURACY_VALUE',
'Maximum model space distance between geometric entities at asserted c
onnectivities');
#23664=(
GEOMETRIC_REPRESENTATION_CONTEXT(3)
GLOBAL_UNCERTAINTY_ASSIGNED_CONTEXT((#23547))
GLOBAL_UNIT_ASSIGNED_CONTEXT((#23729,#23731,#23732))
REPRESENTATION_CONTEXT('','3D')
);
#23728=(
GEOMETRIC_REPRESENTATION_CONTEXT(3)
GLOBAL_UNCERTAINTY_ASSIGNED_CONTEXT((#23611))
GLOBAL_UNIT_ASSIGNED_CONTEXT((#23729,#23731,#23732))
REPRESENTATION_CONTEXT('','3D')
);
#23729=(
LENGTH_UNIT()
NAMED_UNIT(*)
SI_UNIT(.CENTI.,.METRE.)
);
#23731=(
NAMED_UNIT(*)
PLANE_ANGLE_UNIT()
SI_UNIT($,.RADIAN.)
);
#23732=(
NAMED_UNIT(*)
SI_UNIT($,.STERADIAN.)
SOLID_ANGLE_UNIT()
);
#23785=SHAPE_DEFINITION_REPRESENTATION(#23901,#24164);
#23901=PRODUCT_DEFINITION_SHAPE('',$,#24281);
#24164=SHAPE_REPRESENTATION('',(#14467),#23664);
#24228=PRODUCT_DEFINITION_CONTEXT('part definition',#24578,'design');
#24281=PRODUCT_DEFINITION('M4 short cap screw (14)',
'M4 short cap screw (14)',#24397,#24228);
#24397=PRODUCT_DEFINITION_FORMATION('',$,#24632);
#24578=APPLICATION_CONTEXT(
'Core Data for Automotive Mechanical Design Process');
#24579=PRODUCT_CONTEXT('part definition',#24578,'mechanical');
#24632=PRODUCT('M4 short cap screw (14)','M4 short cap screw (14)',
'M4 short cap screw (14)',(#24579));
#24766=COLOUR_RGB('Black',0.12,0.14,0.17);
#24767=FILL_AREA_STYLE_COLOUR('',#24766);
#24768=FILL_AREA_STYLE('',(#24767));
#24769=SURFACE_STYLE_FILL_AREA(#24768);
#24770=SURFACE_SIDE_STYLE('',(#24769));
#24771=SURFACE_STYLE_USAGE(.BOTH.,#24770);
#24772=PRESENTATION_STYLE_ASSIGNMENT((#24771));
ENDSEC;
END-ISO-10303-21;
